ISO-10303-21;
HEADER;
/* Generated by software containing ST-Developer
 * from STEP Tools, Inc. (www.steptools.com) 
 */

FILE_DESCRIPTION(
/* description */ (''),
/* implementation_level */ '2;1');

FILE_NAME(
/* name */ 'Pivot thrust washer.step',
/* time_stamp */ '2026-11-10T05:20:16-08:00',
/* author */ (''),
/* organization */ (''),
/* preprocessor_version */ 'ST-DEVELOPER v20.2',
/* originating_system */ 'Autodesk Translation Framework v15.17.0.0',
/* authorisation */ '');

FILE_SCHEMA (('AUTOMOTIVE_DESIGN { 1 0 10303 214 3 1 1 }'));
ENDSEC;

DATA;
#10=MECHANICAL_DESIGN_GEOMETRIC_PRESENTATION_REPRESENTATION('',(#121),#24809);
#101=SHAPE_REPRESENTATION_RELATIONSHIP('SRR','None',#24865,#111);
#111=ADVANCED_BREP_SHAPE_REPRESENTATION('',(#131),#24808);
#121=STYLED_ITEM('',(#24925),#131);
#131=MANIFOLD_SOLID_BREP('Body1',#9898);
#197=FACE_BOUND('',#2480,.T.);
#198=FACE_BOUND('',#2482,.T.);
#1308=PLANE('',#10663);
#1309=PLANE('',#10664);
#1859=FACE_OUTER_BOUND('',#2477,.T.);
#1860=FACE_OUTER_BOUND('',#2478,.T.);
#1861=FACE_OUTER_BOUND('',#2479,.T.);
#1862=FACE_OUTER_BOUND('',#2481,.T.);
#2477=EDGE_LOOP('',(#9185,#9186,#9187,#9188));
#2478=EDGE_LOOP('',(#9189,#9190,#9191,#9192));
#2479=EDGE_LOOP('',(#9193));
#2480=EDGE_LOOP('',(#9194));
#2481=EDGE_LOOP('',(#9195));
#2482=EDGE_LOOP('',(#9196));
#3069=LINE('',#24766,#3657);
#3070=LINE('',#24772,#3658);
#3657=VECTOR('',#12557,0.41);
#3658=VECTOR('',#12564,0.6);
#3823=CIRCLE('',#10658,0.41);
#3824=CIRCLE('',#10659,0.41);
#3825=CIRCLE('',#10661,0.6);
#3826=CIRCLE('',#10662,0.6);
#4783=VERTEX_POINT('',#24763);
#4784=VERTEX_POINT('',#24765);
#4785=VERTEX_POINT('',#24769);
#4786=VERTEX_POINT('',#24771);
#6251=EDGE_CURVE('',#4783,#4783,#3823,.T.);
#6252=EDGE_CURVE('',#4783,#4784,#3069,.T.);
#6253=EDGE_CURVE('',#4784,#4784,#3824,.T.);
#6254=EDGE_CURVE('',#4785,#4785,#3825,.T.);
#6255=EDGE_CURVE('',#4785,#4786,#3070,.T.);
#6256=EDGE_CURVE('',#4786,#4786,#3826,.T.);
#9185=ORIENTED_EDGE('',*,*,#6251,.F.);
#9186=ORIENTED_EDGE('',*,*,#6252,.T.);
#9187=ORIENTED_EDGE('',*,*,#6253,.T.);
#9188=ORIENTED_EDGE('',*,*,#6252,.F.);
#9189=ORIENTED_EDGE('',*,*,#6254,.F.);
#9190=ORIENTED_EDGE('',*,*,#6255,.T.);
#9191=ORIENTED_EDGE('',*,*,#6256,.T.);
#9192=ORIENTED_EDGE('',*,*,#6255,.F.);
#9193=ORIENTED_EDGE('',*,*,#6254,.T.);
#9194=ORIENTED_EDGE('',*,*,#6251,.T.);
#9195=ORIENTED_EDGE('',*,*,#6256,.F.);
#9196=ORIENTED_EDGE('',*,*,#6253,.F.);
#9334=CYLINDRICAL_SURFACE('',#10657,0.41);
#9335=CYLINDRICAL_SURFACE('',#10660,0.6);
#9885=ADVANCED_FACE('',(#1859),#9334,.F.);
#9886=ADVANCED_FACE('',(#1860),#9335,.T.);
#9887=ADVANCED_FACE('',(#1861,#197),#1308,.T.);
#9888=ADVANCED_FACE('',(#1862,#198),#1309,.F.);
#9898=CLOSED_SHELL('',(#9885,#9886,#9887,#9888));
#10656=AXIS2_PLACEMENT_3D('',#24761,#12551,#12552);
#10657=AXIS2_PLACEMENT_3D('',#24762,#12553,#12554);
#10658=AXIS2_PLACEMENT_3D('',#24764,#12555,#12556);
#10659=AXIS2_PLACEMENT_3D('',#24767,#12558,#12559);
#10660=AXIS2_PLACEMENT_3D('',#24768,#12560,#12561);
#10661=AXIS2_PLACEMENT_3D('',#24770,#12562,#12563);
#10662=AXIS2_PLACEMENT_3D('',#24773,#12565,#12566);
#10663=AXIS2_PLACEMENT_3D('',#24774,#12567,#12568);
#10664=AXIS2_PLACEMENT_3D('',#24775,#12569,#12570);
#12551=DIRECTION('axis',(0.,0.,1.));
#12552=DIRECTION('refdir',(1.,0.,0.));
#12553=DIRECTION('center_axis',(0.,0.,1.));
#12554=DIRECTION('ref_axis',(1.,0.,0.));
#12555=DIRECTION('center_axis',(0.,0.,-1.));
#12556=DIRECTION('ref_axis',(1.,0.,0.));
#12557=DIRECTION('',(0.,0.,-1.));
#12558=DIRECTION('center_axis',(0.,0.,-1.));
#12559=DIRECTION('ref_axis',(1.,0.,0.));
#12560=DIRECTION('center_axis',(0.,0.,1.));
#12561=DIRECTION('ref_axis',(1.,0.,0.));
#12562=DIRECTION('center_axis',(0.,0.,1.));
#12563=DIRECTION('ref_axis',(1.,0.,0.));
#12564=DIRECTION('',(0.,0.,-1.));
#12565=DIRECTION('center_axis',(0.,0.,1.));
#12566=DIRECTION('ref_axis',(1.,0.,0.));
#12567=DIRECTION('center_axis',(0.,0.,1.));
#12568=DIRECTION('ref_axis',(1.,0.,0.));
#12569=DIRECTION('center_axis',(0.,0.,1.));
#12570=DIRECTION('ref_axis',(1.,0.,0.));
#24761=CARTESIAN_POINT('',(0.,0.,0.));
#24762=CARTESIAN_POINT('Origin',(0.,0.,0.));
#24763=CARTESIAN_POINT('',(-0.41,-5.02105187650415E-17,0.1));
#24764=CARTESIAN_POINT('Origin',(0.,0.,0.1));
#24765=CARTESIAN_POINT('',(-0.41,-5.02105187650415E-17,0.));
#24766=CARTESIAN_POINT('',(-0.41,-5.02105187650415E-17,0.));
#24767=CARTESIAN_POINT('Origin',(0.,0.,0.));
#24768=CARTESIAN_POINT('Origin',(0.,0.,0.));
#24769=CARTESIAN_POINT('',(-0.6,-7.34788079488412E-17,0.1));
#24770=CARTESIAN_POINT('Origin',(0.,0.,0.1));
#24771=CARTESIAN_POINT('',(-0.6,-7.34788079488412E-17,0.));
#24772=CARTESIAN_POINT('',(-0.6,-7.34788079488412E-17,0.));
#24773=CARTESIAN_POINT('Origin',(0.,0.,0.));
#24774=CARTESIAN_POINT('Origin',(0.,0.,0.1));
#24775=CARTESIAN_POINT('Origin',(0.,0.,0.));
#24795=UNCERTAINTY_MEASURE_WITH_UNIT(LENGTH_MEASURE(0.001),#24810,
'DISTANCE_ACCURACY_VALUE',
'Maximum model space distance between geometric entities at asserted c
onnectivities');
#24796=UNCERTAINTY_MEASURE_WITH_UNIT(LENGTH_MEASURE(0.001),#24810,
'DISTANCE_ACCURACY_VALUE',
'Maximum model space distance between geometric entities at asserted c
onnectivities');
#24808=(
GEOMETRIC_REPRESENTATION_CONTEXT(3)
GLOBAL_UNCERTAINTY_ASSIGNED_CONTEXT((#24795))
GLOBAL_UNIT_ASSIGNED_CONTEXT((#24810,#24812,#24813))
REPRESENTATION_CONTEXT('','3D')
);
#24809=(
GEOMETRIC_REPRESENTATION_CONTEXT(3)
GLOBAL_UNCERTAINTY_ASSIGNED_CONTEXT((#24796))
GLOBAL_UNIT_ASSIGNED_CONTEXT((#24810,#24812,#24813))
REPRESENTATION_CONTEXT('','3D')
);
#24810=(
LENGTH_UNIT()
NAMED_UNIT(*)
SI_UNIT(.CENTI.,.METRE.)
);
#24812=(
NAMED_UNIT(*)
PLANE_ANGLE_UNIT()
SI_UNIT($,.RADIAN.)
);
#24813=(
NAMED_UNIT(*)
SI_UNIT($,.STERADIAN.)
SOLID_ANGLE_UNIT()
);
#24825=SHAPE_DEFINITION_REPRESENTATION(#24845,#24865);
#24845=PRODUCT_DEFINITION_SHAPE('',$,#24878);
#24865=SHAPE_REPRESENTATION('',(#10656),#24808);
#24866=PRODUCT_DEFINITION_CONTEXT('part definition',#24904,'design');
#24878=PRODUCT_DEFINITION('Pivot thrust washer','Pivot thrust washer',#24890,
#24866);
#24890=PRODUCT_DEFINITION_FORMATION('',$,#24917);
#24904=APPLICATION_CONTEXT(
'Core Data for Automotive Mechanical Design Process');
#24905=PRODUCT_CONTEXT('part definition',#24904,'mechanical');
#24917=PRODUCT('Pivot thrust washer','Pivot thrust washer',$,(#24905));
#24925=PRESENTATION_STYLE_ASSIGNMENT((#24933));
#24933=SURFACE_STYLE_USAGE(.BOTH.,#24941);
#24941=SURFACE_SIDE_STYLE('',(#24949));
#24949=SURFACE_STYLE_FILL_AREA(#24957);
#24957=FILL_AREA_STYLE('Washer gray',(#24965));
#24965=FILL_AREA_STYLE_COLOUR('Washer gray',#24973);
#24973=COLOUR_RGB('Washer gray',0.725490196078431,0.752941176470588,0.792156862745098);
ENDSEC;
END-ISO-10303-21;
